ISO-10303-21;
HEADER;
/* Generated by software containing ST-Developer
 * from STEP Tools, Inc. (www.steptools.com) 
 */

FILE_DESCRIPTION(
/* description */ ('Two-link friction support arm'),
/* implementation_level */ '2;1');

FILE_NAME(
/* name */ 'Hex Nut - M8.step',
/* time_stamp */ '2026-10-27T20:01:49-07:00',
/* author */ (''),
/* organization */ (''),
/* preprocessor_version */ 'ST-DEVELOPER v20.2',
/* originating_system */ 'Autodesk Translation Framework v15.17.0.0',
/* authorisation */ '');

FILE_SCHEMA (('AUTOMOTIVE_DESIGN { 1 0 10303 214 3 1 1 }'));
ENDSEC;

DATA;
#10=MECHANICAL_DESIGN_GEOMETRIC_PRESENTATION_REPRESENTATION('',(#204),#5492);
#149=(
BOUNDED_CURVE()
B_SPLINE_CURVE(2,(#5244,#5245,#5246),.UNSPECIFIED.,.F.,.F.)
B_SPLINE_CURVE_WITH_KNOTS((3,3),(0.14973948338295,0.97160236658079),
 .UNSPECIFIED.)
CURVE()
GEOMETRIC_REPRESENTATION_ITEM()
RATIONAL_B_SPLINE_CURVE((1.07140024848292,1.23714644374248,1.07140024848292))
REPRESENTATION_ITEM('')
);
#150=(
BOUNDED_CURVE()
B_SPLINE_CURVE(2,(#5248,#5249,#5250),.UNSPECIFIED.,.F.,.F.)
B_SPLINE_CURVE_WITH_KNOTS((3,3),(0.14973948338295,0.971602366580789),
 .UNSPECIFIED.)
CURVE()
GEOMETRIC_REPRESENTATION_ITEM()
RATIONAL_B_SPLINE_CURVE((1.07140024848292,1.23714644374248,1.07140024848292))
REPRESENTATION_ITEM('')
);
#151=(
BOUNDED_CURVE()
B_SPLINE_CURVE(2,(#5255,#5256,#5257),.UNSPECIFIED.,.F.,.F.)
B_SPLINE_CURVE_WITH_KNOTS((3,3),(0.14973948338295,0.97160236658079),
 .UNSPECIFIED.)
CURVE()
GEOMETRIC_REPRESENTATION_ITEM()
RATIONAL_B_SPLINE_CURVE((1.07140024848292,1.23714644374248,1.07140024848292))
REPRESENTATION_ITEM('')
);
#152=(
BOUNDED_CURVE()
B_SPLINE_CURVE(2,(#5259,#5260,#5261),.UNSPECIFIED.,.F.,.F.)
B_SPLINE_CURVE_WITH_KNOTS((3,3),(0.14973948338295,0.97160236658079),
 .UNSPECIFIED.)
CURVE()
GEOMETRIC_REPRESENTATION_ITEM()
RATIONAL_B_SPLINE_CURVE((1.07140024848292,1.23714644374248,1.07140024848292))
REPRESENTATION_ITEM('')
);
#153=(
BOUNDED_CURVE()
B_SPLINE_CURVE(2,(#5263,#5264,#5265),.UNSPECIFIED.,.F.,.F.)
B_SPLINE_CURVE_WITH_KNOTS((3,3),(0.14973948338295,0.971602366580789),
 .UNSPECIFIED.)
CURVE()
GEOMETRIC_REPRESENTATION_ITEM()
RATIONAL_B_SPLINE_CURVE((1.07140024848292,1.23714644374248,1.07140024848292))
REPRESENTATION_ITEM('')
);
#154=(
BOUNDED_CURVE()
B_SPLINE_CURVE(2,(#5266,#5267,#5268),.UNSPECIFIED.,.F.,.F.)
B_SPLINE_CURVE_WITH_KNOTS((3,3),(0.14973948338295,0.97160236658079),
 .UNSPECIFIED.)
CURVE()
GEOMETRIC_REPRESENTATION_ITEM()
RATIONAL_B_SPLINE_CURVE((1.07140024848292,1.23714644374248,1.07140024848292))
REPRESENTATION_ITEM('')
);
#155=(
BOUNDED_CURVE()
B_SPLINE_CURVE(2,(#5275,#5276,#5277),.UNSPECIFIED.,.F.,.F.)
B_SPLINE_CURVE_WITH_KNOTS((3,3),(0.14973948338295,0.97160236658079),
 .UNSPECIFIED.)
CURVE()
GEOMETRIC_REPRESENTATION_ITEM()
RATIONAL_B_SPLINE_CURVE((1.07140024848292,1.23714644374248,1.07140024848292))
REPRESENTATION_ITEM('')
);
#156=(
BOUNDED_CURVE()
B_SPLINE_CURVE(2,(#5279,#5280,#5281),.UNSPECIFIED.,.F.,.F.)
B_SPLINE_CURVE_WITH_KNOTS((3,3),(0.14973948338295,0.97160236658079),
 .UNSPECIFIED.)
CURVE()
GEOMETRIC_REPRESENTATION_ITEM()
RATIONAL_B_SPLINE_CURVE((1.07140024848292,1.23714644374248,1.07140024848292))
REPRESENTATION_ITEM('')
);
#157=(
BOUNDED_CURVE()
B_SPLINE_CURVE(2,(#5283,#5284,#5285),.UNSPECIFIED.,.F.,.F.)
B_SPLINE_CURVE_WITH_KNOTS((3,3),(0.14973948338295,0.971602366580789),
 .UNSPECIFIED.)
CURVE()
GEOMETRIC_REPRESENTATION_ITEM()
RATIONAL_B_SPLINE_CURVE((1.07140024848292,1.23714644374248,1.07140024848292))
REPRESENTATION_ITEM('')
);
#158=(
BOUNDED_CURVE()
B_SPLINE_CURVE(2,(#5287,#5288,#5289),.UNSPECIFIED.,.F.,.F.)
B_SPLINE_CURVE_WITH_KNOTS((3,3),(0.14973948338295,0.97160236658079),
 .UNSPECIFIED.)
CURVE()
GEOMETRIC_REPRESENTATION_ITEM()
RATIONAL_B_SPLINE_CURVE((1.07140024848292,1.23714644374248,1.07140024848292))
REPRESENTATION_ITEM('')
);
#159=(
BOUNDED_CURVE()
B_SPLINE_CURVE(2,(#5291,#5292,#5293),.UNSPECIFIED.,.F.,.F.)
B_SPLINE_CURVE_WITH_KNOTS((3,3),(0.14973948338295,0.97160236658079),
 .UNSPECIFIED.)
CURVE()
GEOMETRIC_REPRESENTATION_ITEM()
RATIONAL_B_SPLINE_CURVE((1.07140024848292,1.23714644374248,1.07140024848292))
REPRESENTATION_ITEM('')
);
#160=(
BOUNDED_CURVE()
B_SPLINE_CURVE(2,(#5294,#5295,#5296),.UNSPECIFIED.,.F.,.F.)
B_SPLINE_CURVE_WITH_KNOTS((3,3),(0.14973948338295,0.971602366580789),
 .UNSPECIFIED.)
CURVE()
GEOMETRIC_REPRESENTATION_ITEM()
RATIONAL_B_SPLINE_CURVE((1.07140024848292,1.23714644374248,1.07140024848292))
REPRESENTATION_ITEM('')
);
#169=CONICAL_SURFACE('',#3517,0.734027674973257,1.0471975511966);
#170=CONICAL_SURFACE('',#3519,0.734027674973257,1.0471975511966);
#182=SHAPE_REPRESENTATION_RELATIONSHIP('SRR','None',#5576,#193);
#193=ADVANCED_BREP_SHAPE_REPRESENTATION('',(#214),#5490);
#204=STYLED_ITEM('',(#5708),#214);
#214=MANIFOLD_SOLID_BREP('Body1',#3181);
#245=FACE_BOUND('',#713,.T.);
#246=FACE_BOUND('',#715,.T.);
#356=PLANE('',#3521);
#357=PLANE('',#3522);
#358=PLANE('',#3523);
#359=PLANE('',#3527);
#360=PLANE('',#3528);
#361=PLANE('',#3529);
#362=PLANE('',#3530);
#363=PLANE('',#3531);
#507=FACE_OUTER_BOUND('',#703,.T.);
#508=FACE_OUTER_BOUND('',#704,.T.);
#509=FACE_OUTER_BOUND('',#705,.T.);
#510=FACE_OUTER_BOUND('',#706,.T.);
#511=FACE_OUTER_BOUND('',#707,.T.);
#512=FACE_OUTER_BOUND('',#708,.T.);
#513=FACE_OUTER_BOUND('',#709,.T.);
#514=FACE_OUTER_BOUND('',#710,.T.);
#515=FACE_OUTER_BOUND('',#711,.T.);
#516=FACE_OUTER_BOUND('',#712,.T.);
#517=FACE_OUTER_BOUND('',#714,.T.);
#703=EDGE_LOOP('',(#2804,#2805,#2806,#2807,#2808,#2809,#2810,#2811,#2812));
#704=EDGE_LOOP('',(#2813,#2814,#2815,#2816,#2817,#2818,#2819,#2820,#2821));
#705=EDGE_LOOP('',(#2822,#2823,#2824,#2825));
#706=EDGE_LOOP('',(#2826,#2827,#2828,#2829));
#707=EDGE_LOOP('',(#2830,#2831,#2832,#2833));
#708=EDGE_LOOP('',(#2834,#2835,#2836,#2837));
#709=EDGE_LOOP('',(#2838,#2839,#2840,#2841));
#710=EDGE_LOOP('',(#2842,#2843,#2844,#2845));
#711=EDGE_LOOP('',(#2846,#2847,#2848,#2849));
#712=EDGE_LOOP('',(#2850));
#713=EDGE_LOOP('',(#2851));
#714=EDGE_LOOP('',(#2852));
#715=EDGE_LOOP('',(#2853));
#1014=LINE('',#5252,#1327);
#1015=LINE('',#5273,#1328);
#1016=LINE('',#5298,#1329);
#1017=LINE('',#5299,#1330);
#1018=LINE('',#5301,#1331);
#1019=LINE('',#5303,#1332);
#1020=LINE('',#5308,#1333);
#1021=LINE('',#5311,#1334);
#1022=LINE('',#5313,#1335);
#1327=VECTOR('',#4304,0.734027674973257);
#1328=VECTOR('',#4311,0.734027674973257);
#1329=VECTOR('',#4314,1.);
#1330=VECTOR('',#4315,1.);
#1331=VECTOR('',#4318,1.);
#1332=VECTOR('',#4321,1.);
#1333=VECTOR('',#4326,0.4);
#1334=VECTOR('',#4331,1.);
#1335=VECTOR('',#4334,1.);
#1419=CIRCLE('',#3518,0.6175);
#1420=CIRCLE('',#3520,0.6175);
#1421=CIRCLE('',#3525,0.338975);
#1422=CIRCLE('',#3526,0.338975);
#1669=VERTEX_POINT('',#5242);
#1670=VERTEX_POINT('',#5243);
#1671=VERTEX_POINT('',#5247);
#1672=VERTEX_POINT('',#5251);
#1673=VERTEX_POINT('',#5254);
#1674=VERTEX_POINT('',#5258);
#1675=VERTEX_POINT('',#5262);
#1676=VERTEX_POINT('',#5270);
#1677=VERTEX_POINT('',#5272);
#1678=VERTEX_POINT('',#5274);
#1679=VERTEX_POINT('',#5278);
#1680=VERTEX_POINT('',#5282);
#1681=VERTEX_POINT('',#5286);
#1682=VERTEX_POINT('',#5290);
#1683=VERTEX_POINT('',#5305);
#1684=VERTEX_POINT('',#5307);
#2056=EDGE_CURVE('',#1669,#1670,#149,.T.);
#2057=EDGE_CURVE('',#1671,#1669,#150,.T.);
#2058=EDGE_CURVE('',#1671,#1672,#1014,.T.);
#2059=EDGE_CURVE('',#1672,#1672,#1419,.T.);
#2060=EDGE_CURVE('',#1673,#1671,#151,.T.);
#2061=EDGE_CURVE('',#1674,#1673,#152,.T.);
#2062=EDGE_CURVE('',#1675,#1674,#153,.T.);
#2063=EDGE_CURVE('',#1670,#1675,#154,.T.);
#2064=EDGE_CURVE('',#1676,#1676,#1420,.T.);
#2065=EDGE_CURVE('',#1676,#1677,#1015,.T.);
#2066=EDGE_CURVE('',#1678,#1677,#155,.T.);
#2067=EDGE_CURVE('',#1679,#1678,#156,.T.);
#2068=EDGE_CURVE('',#1680,#1679,#157,.T.);
#2069=EDGE_CURVE('',#1681,#1680,#158,.T.);
#2070=EDGE_CURVE('',#1682,#1681,#159,.T.);
#2071=EDGE_CURVE('',#1677,#1682,#160,.T.);
#2072=EDGE_CURVE('',#1673,#1682,#1016,.T.);
#2073=EDGE_CURVE('',#1674,#1681,#1017,.T.);
#2074=EDGE_CURVE('',#1671,#1677,#1018,.T.);
#2075=EDGE_CURVE('',#1669,#1678,#1019,.T.);
#2076=EDGE_CURVE('',#1683,#1683,#1421,.F.);
#2077=EDGE_CURVE('',#1683,#1684,#1020,.T.);
#2078=EDGE_CURVE('',#1684,#1684,#1422,.F.);
#2079=EDGE_CURVE('',#1670,#1679,#1021,.T.);
#2080=EDGE_CURVE('',#1675,#1680,#1022,.T.);
#2804=ORIENTED_EDGE('',*,*,#2056,.F.);
#2805=ORIENTED_EDGE('',*,*,#2057,.F.);
#2806=ORIENTED_EDGE('',*,*,#2058,.T.);
#2807=ORIENTED_EDGE('',*,*,#2059,.F.);
#2808=ORIENTED_EDGE('',*,*,#2058,.F.);
#2809=ORIENTED_EDGE('',*,*,#2060,.F.);
#2810=ORIENTED_EDGE('',*,*,#2061,.F.);
#2811=ORIENTED_EDGE('',*,*,#2062,.F.);
#2812=ORIENTED_EDGE('',*,*,#2063,.F.);
#2813=ORIENTED_EDGE('',*,*,#2064,.F.);
#2814=ORIENTED_EDGE('',*,*,#2065,.T.);
#2815=ORIENTED_EDGE('',*,*,#2066,.F.);
#2816=ORIENTED_EDGE('',*,*,#2067,.F.);
#2817=ORIENTED_EDGE('',*,*,#2068,.F.);
#2818=ORIENTED_EDGE('',*,*,#2069,.F.);
#2819=ORIENTED_EDGE('',*,*,#2070,.F.);
#2820=ORIENTED_EDGE('',*,*,#2071,.F.);
#2821=ORIENTED_EDGE('',*,*,#2065,.F.);
#2822=ORIENTED_EDGE('',*,*,#2061,.T.);
#2823=ORIENTED_EDGE('',*,*,#2072,.T.);
#2824=ORIENTED_EDGE('',*,*,#2070,.T.);
#2825=ORIENTED_EDGE('',*,*,#2073,.F.);
#2826=ORIENTED_EDGE('',*,*,#2060,.T.);
#2827=ORIENTED_EDGE('',*,*,#2074,.T.);
#2828=ORIENTED_EDGE('',*,*,#2071,.T.);
#2829=ORIENTED_EDGE('',*,*,#2072,.F.);
#2830=ORIENTED_EDGE('',*,*,#2057,.T.);
#2831=ORIENTED_EDGE('',*,*,#2075,.T.);
#2832=ORIENTED_EDGE('',*,*,#2066,.T.);
#2833=ORIENTED_EDGE('',*,*,#2074,.F.);
#2834=ORIENTED_EDGE('',*,*,#2076,.F.);
#2835=ORIENTED_EDGE('',*,*,#2077,.T.);
#2836=ORIENTED_EDGE('',*,*,#2078,.T.);
#2837=ORIENTED_EDGE('',*,*,#2077,.F.);
#2838=ORIENTED_EDGE('',*,*,#2056,.T.);
#2839=ORIENTED_EDGE('',*,*,#2079,.T.);
#2840=ORIENTED_EDGE('',*,*,#2067,.T.);
#2841=ORIENTED_EDGE('',*,*,#2075,.F.);
#2842=ORIENTED_EDGE('',*,*,#2062,.T.);
#2843=ORIENTED_EDGE('',*,*,#2073,.T.);
#2844=ORIENTED_EDGE('',*,*,#2069,.T.);
#2845=ORIENTED_EDGE('',*,*,#2080,.F.);
#2846=ORIENTED_EDGE('',*,*,#2063,.T.);
#2847=ORIENTED_EDGE('',*,*,#2080,.T.);
#2848=ORIENTED_EDGE('',*,*,#2068,.T.);
#2849=ORIENTED_EDGE('',*,*,#2079,.F.);
#2850=ORIENTED_EDGE('',*,*,#2064,.T.);
#2851=ORIENTED_EDGE('',*,*,#2076,.T.);
#2852=ORIENTED_EDGE('',*,*,#2059,.T.);
#2853=ORIENTED_EDGE('',*,*,#2078,.F.);
#2990=CYLINDRICAL_SURFACE('',#3524,0.338975);
#3138=ADVANCED_FACE('',(#507),#169,.T.);
#3139=ADVANCED_FACE('',(#508),#170,.T.);
#3140=ADVANCED_FACE('',(#509),#356,.T.);
#3141=ADVANCED_FACE('',(#510),#357,.T.);
#3142=ADVANCED_FACE('',(#511),#358,.T.);
#3143=ADVANCED_FACE('',(#512),#2990,.F.);
#3144=ADVANCED_FACE('',(#513),#359,.T.);
#3145=ADVANCED_FACE('',(#514),#360,.T.);
#3146=ADVANCED_FACE('',(#515),#361,.T.);
#3147=ADVANCED_FACE('',(#516,#245),#362,.T.);
#3148=ADVANCED_FACE('',(#517,#246),#363,.F.);
#3181=CLOSED_SHELL('',(#3138,#3139,#3140,#3141,#3142,#3143,#3144,#3145,
#3146,#3147,#3148));
#3516=AXIS2_PLACEMENT_3D('',#5240,#4300,#4301);
#3517=AXIS2_PLACEMENT_3D('',#5241,#4302,#4303);
#3518=AXIS2_PLACEMENT_3D('',#5253,#4305,#4306);
#3519=AXIS2_PLACEMENT_3D('',#5269,#4307,#4308);
#3520=AXIS2_PLACEMENT_3D('',#5271,#4309,#4310);
#3521=AXIS2_PLACEMENT_3D('',#5297,#4312,#4313);
#3522=AXIS2_PLACEMENT_3D('',#5300,#4316,#4317);
#3523=AXIS2_PLACEMENT_3D('',#5302,#4319,#4320);
#3524=AXIS2_PLACEMENT_3D('',#5304,#4322,#4323);
#3525=AXIS2_PLACEMENT_3D('',#5306,#4324,#4325);
#3526=AXIS2_PLACEMENT_3D('',#5309,#4327,#4328);
#3527=AXIS2_PLACEMENT_3D('',#5310,#4329,#4330);
#3528=AXIS2_PLACEMENT_3D('',#5312,#4332,#4333);
#3529=AXIS2_PLACEMENT_3D('',#5314,#4335,#4336);
#3530=AXIS2_PLACEMENT_3D('',#5315,#4337,#4338);
#3531=AXIS2_PLACEMENT_3D('',#5316,#4339,#4340);
#4300=DIRECTION('axis',(0.,0.,1.));
#4301=DIRECTION('refdir',(1.,0.,0.));
#4302=DIRECTION('center_axis',(0.,1.,0.));
#4303=DIRECTION('ref_axis',(1.,0.,0.));
#4304=DIRECTION('',(0.866025403784439,-0.5,1.06057523872491E-16));
#4305=DIRECTION('center_axis',(0.,-1.,0.));
#4306=DIRECTION('ref_axis',(1.,0.,0.));
#4307=DIRECTION('center_axis',(0.,-1.,0.));
#4308=DIRECTION('ref_axis',(1.,0.,0.));
#4309=DIRECTION('center_axis',(0.,1.,0.));
#4310=DIRECTION('ref_axis',(1.,0.,0.));
#4311=DIRECTION('',(-0.866025403784439,-0.5,-1.06057523872491E-16));
#4312=DIRECTION('center_axis',(1.4792020664489E-16,0.,-1.));
#4313=DIRECTION('ref_axis',(-1.,0.,-1.4792020664489E-16));
#4314=DIRECTION('',(0.,1.,0.));
#4315=DIRECTION('',(0.,1.,0.));
#4316=DIRECTION('center_axis',(-0.866025403784439,0.,-0.5));
#4317=DIRECTION('ref_axis',(-0.5,0.,0.866025403784439));
#4318=DIRECTION('',(0.,1.,0.));
#4319=DIRECTION('center_axis',(-0.866025403784439,0.,0.5));
#4320=DIRECTION('ref_axis',(0.5,0.,0.866025403784439));
#4321=DIRECTION('',(0.,1.,0.));
#4322=DIRECTION('center_axis',(0.,1.,0.));
#4323=DIRECTION('ref_axis',(1.,0.,0.));
#4324=DIRECTION('center_axis',(0.,1.,0.));
#4325=DIRECTION('ref_axis',(1.,0.,0.));
#4326=DIRECTION('',(0.,-1.,0.));
#4327=DIRECTION('center_axis',(0.,1.,0.));
#4328=DIRECTION('ref_axis',(1.,0.,0.));
#4329=DIRECTION('center_axis',(-2.95840413289779E-16,0.,1.));
#4330=DIRECTION('ref_axis',(1.,0.,2.95840413289779E-16));
#4331=DIRECTION('',(0.,1.,0.));
#4332=DIRECTION('center_axis',(0.866025403784439,0.,-0.5));
#4333=DIRECTION('ref_axis',(-0.5,0.,-0.866025403784439));
#4334=DIRECTION('',(0.,1.,0.));
#4335=DIRECTION('center_axis',(0.866025403784439,0.,0.5));
#4336=DIRECTION('ref_axis',(0.5,0.,-0.866025403784439));
#4337=DIRECTION('center_axis',(0.,1.,0.));
#4338=DIRECTION('ref_axis',(1.,0.,0.));
#4339=DIRECTION('center_axis',(0.,1.,0.));
#4340=DIRECTION('ref_axis',(1.,0.,0.));
#5240=CARTESIAN_POINT('',(0.,0.,0.));
#5241=CARTESIAN_POINT('Origin',(0.,0.067277284513851,0.));
#5242=CARTESIAN_POINT('',(-0.375277674973257,0.0768195421087395,0.65));
#5243=CARTESIAN_POINT('',(0.375277674973257,0.0768195421087395,0.65));
#5244=CARTESIAN_POINT('Ctrl Pts',(-0.375277674973257,0.0768195421087395,
0.65));
#5245=CARTESIAN_POINT('Ctrl Pts',(1.66533453693773E-13,-0.0315137912242439,
0.65));
#5246=CARTESIAN_POINT('Ctrl Pts',(0.375277674973257,0.0768195421087394,
0.65));
#5247=CARTESIAN_POINT('',(-0.750555349946514,0.0768195421087394,-9.19165206894919E-17));
#5248=CARTESIAN_POINT('Ctrl Pts',(-0.750555349946514,0.0768195421087394,
-9.19165206894919E-17));
#5249=CARTESIAN_POINT('Ctrl Pts',(-0.562916512459802,-0.0315137912242434,
0.325000000000144));
#5250=CARTESIAN_POINT('Ctrl Pts',(-0.375277674973257,0.0768195421087395,
0.65));
#5251=CARTESIAN_POINT('',(-0.6175,-2.77555756156289E-17,-7.5621939847349E-17));
#5252=CARTESIAN_POINT('',(-0.734027674973257,0.067277284513851,-8.98924642641573E-17));
#5253=CARTESIAN_POINT('Origin',(0.,0.,0.));
#5254=CARTESIAN_POINT('',(-0.375277674973257,0.0768195421087395,-0.65));
#5255=CARTESIAN_POINT('Ctrl Pts',(-0.375277674973257,0.0768195421087395,
-0.65));
#5256=CARTESIAN_POINT('Ctrl Pts',(-0.562916512459968,-0.0315137912242437,
-0.324999999999856));
#5257=CARTESIAN_POINT('Ctrl Pts',(-0.750555349946514,0.0768195421087395,
-9.19165206894919E-17));
#5258=CARTESIAN_POINT('',(0.375277674973257,0.0768195421087395,-0.65));
#5259=CARTESIAN_POINT('Ctrl Pts',(0.375277674973257,0.0768195421087395,
-0.65));
#5260=CARTESIAN_POINT('Ctrl Pts',(-1.66144875635155E-13,-0.0315137912242437,
-0.65));
#5261=CARTESIAN_POINT('Ctrl Pts',(-0.375277674973257,0.0768195421087395,
-0.65));
#5262=CARTESIAN_POINT('',(0.750555349946514,0.0768195421087394,0.));
#5263=CARTESIAN_POINT('Ctrl Pts',(0.750555349946514,0.0768195421087394,
0.));
#5264=CARTESIAN_POINT('Ctrl Pts',(0.562916512459802,-0.0315137912242436,
-0.325000000000144));
#5265=CARTESIAN_POINT('Ctrl Pts',(0.375277674973257,0.0768195421087395,
-0.65));
#5266=CARTESIAN_POINT('Ctrl Pts',(0.375277674973257,0.0768195421087394,
0.65));
#5267=CARTESIAN_POINT('Ctrl Pts',(0.562916512459968,-0.0315137912242439,
0.324999999999856));
#5268=CARTESIAN_POINT('Ctrl Pts',(0.750555349946514,0.0768195421087394,
0.));
#5269=CARTESIAN_POINT('Origin',(0.,0.612722715486149,0.));
#5270=CARTESIAN_POINT('',(-0.6175,0.68,-7.5621939847349E-17));
#5271=CARTESIAN_POINT('Origin',(0.,0.68,0.));
#5272=CARTESIAN_POINT('',(-0.750555349946514,0.603180457891261,-9.19165206894919E-17));
#5273=CARTESIAN_POINT('',(-0.734027674973257,0.612722715486149,-8.98924642641573E-17));
#5274=CARTESIAN_POINT('',(-0.375277674973257,0.603180457891261,0.65));
#5275=CARTESIAN_POINT('Ctrl Pts',(-0.375277674973257,0.603180457891261,
0.65));
#5276=CARTESIAN_POINT('Ctrl Pts',(-0.562916512459968,0.711513791224243,
0.324999999999856));
#5277=CARTESIAN_POINT('Ctrl Pts',(-0.750555349946514,0.603180457891261,
-9.19165206894919E-17));
#5278=CARTESIAN_POINT('',(0.375277674973257,0.603180457891261,0.65));
#5279=CARTESIAN_POINT('Ctrl Pts',(0.375277674973257,0.603180457891261,0.65));
#5280=CARTESIAN_POINT('Ctrl Pts',(-1.66755498298699E-13,0.711513791224244,
0.65));
#5281=CARTESIAN_POINT('Ctrl Pts',(-0.375277674973257,0.603180457891261,
0.65));
#5282=CARTESIAN_POINT('',(0.750555349946514,0.603180457891261,0.));
#5283=CARTESIAN_POINT('Ctrl Pts',(0.750555349946514,0.603180457891261,0.));
#5284=CARTESIAN_POINT('Ctrl Pts',(0.562916512459802,0.711513791224244,0.325000000000144));
#5285=CARTESIAN_POINT('Ctrl Pts',(0.375277674973257,0.603180457891261,0.65));
#5286=CARTESIAN_POINT('',(0.375277674973257,0.603180457891261,-0.65));
#5287=CARTESIAN_POINT('Ctrl Pts',(0.375277674973257,0.603180457891261,-0.65));
#5288=CARTESIAN_POINT('Ctrl Pts',(0.562916512459969,0.711513791224244,-0.324999999999856));
#5289=CARTESIAN_POINT('Ctrl Pts',(0.750555349946514,0.603180457891261,0.));
#5290=CARTESIAN_POINT('',(-0.375277674973257,0.603180457891261,-0.65));
#5291=CARTESIAN_POINT('Ctrl Pts',(-0.375277674973257,0.603180457891261,
-0.65));
#5292=CARTESIAN_POINT('Ctrl Pts',(1.66422431391311E-13,0.711513791224244,
-0.65));
#5293=CARTESIAN_POINT('Ctrl Pts',(0.375277674973257,0.603180457891261,-0.65));
#5294=CARTESIAN_POINT('Ctrl Pts',(-0.750555349946514,0.603180457891261,
-9.19165206894919E-17));
#5295=CARTESIAN_POINT('Ctrl Pts',(-0.562916512459802,0.711513791224244,
-0.325000000000144));
#5296=CARTESIAN_POINT('Ctrl Pts',(-0.375277674973257,0.603180457891261,
-0.65));
#5297=CARTESIAN_POINT('Origin',(0.375277674973257,0.,-0.65));
#5298=CARTESIAN_POINT('',(-0.375277674973257,0.,-0.65));
#5299=CARTESIAN_POINT('',(0.375277674973257,0.,-0.65));
#5300=CARTESIAN_POINT('Origin',(-0.375277674973257,0.,-0.65));
#5301=CARTESIAN_POINT('',(-0.750555349946514,0.,-9.19165206894919E-17));
#5302=CARTESIAN_POINT('Origin',(-0.750555349946514,0.,-9.19165206894919E-17));
#5303=CARTESIAN_POINT('',(-0.375277674973257,0.,0.65));
#5304=CARTESIAN_POINT('Origin',(0.,0.,0.));
#5305=CARTESIAN_POINT('',(-0.338975,0.68,4.15124648740974E-17));
#5306=CARTESIAN_POINT('Origin',(0.,0.68,0.));
#5307=CARTESIAN_POINT('',(-0.338975,0.,4.15124648740974E-17));
#5308=CARTESIAN_POINT('',(-0.338975,0.,4.15124648740974E-17));
#5309=CARTESIAN_POINT('Origin',(0.,0.,0.));
#5310=CARTESIAN_POINT('Origin',(-0.375277674973257,0.,0.65));
#5311=CARTESIAN_POINT('',(0.375277674973257,0.,0.65));
#5312=CARTESIAN_POINT('Origin',(0.750555349946514,0.,0.));
#5313=CARTESIAN_POINT('',(0.750555349946514,0.,0.));
#5314=CARTESIAN_POINT('Origin',(0.375277674973257,0.,0.65));
#5315=CARTESIAN_POINT('Origin',(0.,0.68,-1.11022302462516E-16));
#5316=CARTESIAN_POINT('Origin',(0.,0.,-1.11022302462516E-16));
#5473=UNCERTAINTY_MEASURE_WITH_UNIT(LENGTH_MEASURE(0.001),#5493,
'DISTANCE_ACCURACY_VALUE',
'Maximum model space distance between geometric entities at asserted c
onnectivities');
#5475=UNCERTAINTY_MEASURE_WITH_UNIT(LENGTH_MEASURE(0.001),#5493,
'DISTANCE_ACCURACY_VALUE',
'Maximum model space distance between geometric entities at asserted c
onnectivities');
#5490=(
GEOMETRIC_REPRESENTATION_CONTEXT(3)
GLOBAL_UNCERTAINTY_ASSIGNED_CONTEXT((#5473))
GLOBAL_UNIT_ASSIGNED_CONTEXT((#5493,#5495,#5496))
REPRESENTATION_CONTEXT('','3D')
);
#5492=(
GEOMETRIC_REPRESENTATION_CONTEXT(3)
GLOBAL_UNCERTAINTY_ASSIGNED_CONTEXT((#5475))
GLOBAL_UNIT_ASSIGNED_CONTEXT((#5493,#5495,#5496))
REPRESENTATION_CONTEXT('','3D')
);
#5493=(
LENGTH_UNIT()
NAMED_UNIT(*)
SI_UNIT(.CENTI.,.METRE.)
);
#5495=(
NAMED_UNIT(*)
PLANE_ANGLE_UNIT()
SI_UNIT($,.RADIAN.)
);
#5496=(
NAMED_UNIT(*)
SI_UNIT($,.STERADIAN.)
SOLID_ANGLE_UNIT()
);
#5511=SHAPE_DEFINITION_REPRESENTATION(#5536,#5576);
#5536=PRODUCT_DEFINITION_SHAPE('',$,#5593);
#5576=SHAPE_REPRESENTATION('',(#3516),#5490);
#5578=PRODUCT_DEFINITION_CONTEXT('part definition',#5628,'design');
#5593=PRODUCT_DEFINITION('Hex Nut - M8','Hex Nut - M8',#5609,#5578);
#5609=PRODUCT_DEFINITION_FORMATION('',$,#5644);
#5628=APPLICATION_CONTEXT(
'Core Data for Automotive Mechanical Design Process');
#5629=PRODUCT_CONTEXT('part definition',#5628,'mechanical');
#5644=PRODUCT('Hex Nut - M8','Hex Nut - M8','Hex Nut - M8',(#5629));
#5702=COLOUR_RGB('Black',0.12,0.14,0.17);
#5703=FILL_AREA_STYLE_COLOUR('',#5702);
#5704=FILL_AREA_STYLE('',(#5703));
#5705=SURFACE_STYLE_FILL_AREA(#5704);
#5706=SURFACE_SIDE_STYLE('',(#5705));
#5707=SURFACE_STYLE_USAGE(.BOTH.,#5706);
#5708=PRESENTATION_STYLE_ASSIGNMENT((#5707));
ENDSEC;
END-ISO-10303-21;
